ISO-10303-21;
HEADER;
/* Generated by software containing ST-Developer
 * from STEP Tools, Inc. (www.steptools.com) 
 */

FILE_DESCRIPTION(
/* description */ ('Rigid flange shaft coupling assembly'),
/* implementation_level */ '2;1');

FILE_NAME(
/* name */ 'Mounting bush (1).step',
/* time_stamp */ '2026-10-27T10:47:16-07:00',
/* author */ (''),
/* organization */ (''),
/* preprocessor_version */ 'ST-DEVELOPER v20.2',
/* originating_system */ 'Autodesk Translation Framework v15.17.0.0',
/* authorisation */ '');

FILE_SCHEMA (('AUTOMOTIVE_DESIGN { 1 0 10303 214 3 1 1 }'));
ENDSEC;

DATA;
#10=MECHANICAL_DESIGN_GEOMETRIC_PRESENTATION_REPRESENTATION('',(#403),#9141);
#347=SHAPE_REPRESENTATION_RELATIONSHIP('SRR','None',#9281,#375);
#375=ADVANCED_BREP_SHAPE_REPRESENTATION('',(#432),#9116);
#403=STYLED_ITEM('',(#9493),#432);
#432=MANIFOLD_SOLID_BREP('Body1',#4757);
#471=FACE_BOUND('',#1073,.T.);
#472=FACE_BOUND('',#1075,.T.);
#596=PLANE('',#5163);
#597=PLANE('',#5164);
#780=FACE_OUTER_BOUND('',#1070,.T.);
#781=FACE_OUTER_BOUND('',#1071,.T.);
#782=FACE_OUTER_BOUND('',#1072,.T.);
#783=FACE_OUTER_BOUND('',#1074,.T.);
#1070=EDGE_LOOP('',(#3399,#3400,#3401,#3402));
#1071=EDGE_LOOP('',(#3403,#3404,#3405,#3406));
#1072=EDGE_LOOP('',(#3407));
#1073=EDGE_LOOP('',(#3408));
#1074=EDGE_LOOP('',(#3409));
#1075=EDGE_LOOP('',(#3410));
#1463=LINE('',#7263,#1808);
#1464=LINE('',#7269,#1809);
#1808=VECTOR('',#5832,0.425);
#1809=VECTOR('',#5839,0.645);
#2115=CIRCLE('',#5158,0.425);
#2116=CIRCLE('',#5159,0.425);
#2117=CIRCLE('',#5161,0.645);
#2118=CIRCLE('',#5162,0.645);
#2328=VERTEX_POINT('',#7260);
#2329=VERTEX_POINT('',#7262);
#2330=VERTEX_POINT('',#7266);
#2331=VERTEX_POINT('',#7268);
#2743=EDGE_CURVE('',#2328,#2328,#2115,.T.);
#2744=EDGE_CURVE('',#2328,#2329,#1463,.T.);
#2745=EDGE_CURVE('',#2329,#2329,#2116,.T.);
#2746=EDGE_CURVE('',#2330,#2330,#2117,.T.);
#2747=EDGE_CURVE('',#2330,#2331,#1464,.T.);
#2748=EDGE_CURVE('',#2331,#2331,#2118,.T.);
#3399=ORIENTED_EDGE('',*,*,#2743,.F.);
#3400=ORIENTED_EDGE('',*,*,#2744,.T.);
#3401=ORIENTED_EDGE('',*,*,#2745,.T.);
#3402=ORIENTED_EDGE('',*,*,#2744,.F.);
#3403=ORIENTED_EDGE('',*,*,#2746,.F.);
#3404=ORIENTED_EDGE('',*,*,#2747,.T.);
#3405=ORIENTED_EDGE('',*,*,#2748,.T.);
#3406=ORIENTED_EDGE('',*,*,#2747,.F.);
#3407=ORIENTED_EDGE('',*,*,#2746,.T.);
#3408=ORIENTED_EDGE('',*,*,#2743,.T.);
#3409=ORIENTED_EDGE('',*,*,#2748,.F.);
#3410=ORIENTED_EDGE('',*,*,#2745,.F.);
#4409=CYLINDRICAL_SURFACE('',#5157,0.425);
#4410=CYLINDRICAL_SURFACE('',#5160,0.645);
#4516=ADVANCED_FACE('',(#780),#4409,.F.);
#4517=ADVANCED_FACE('',(#781),#4410,.T.);
#4518=ADVANCED_FACE('',(#782,#471),#596,.T.);
#4519=ADVANCED_FACE('',(#783,#472),#597,.F.);
#4757=CLOSED_SHELL('',(#4516,#4517,#4518,#4519));
#5156=AXIS2_PLACEMENT_3D('',#7258,#5826,#5827);
#5157=AXIS2_PLACEMENT_3D('',#7259,#5828,#5829);
#5158=AXIS2_PLACEMENT_3D('',#7261,#5830,#5831);
#5159=AXIS2_PLACEMENT_3D('',#7264,#5833,#5834);
#5160=AXIS2_PLACEMENT_3D('',#7265,#5835,#5836);
#5161=AXIS2_PLACEMENT_3D('',#7267,#5837,#5838);
#5162=AXIS2_PLACEMENT_3D('',#7270,#5840,#5841);
#5163=AXIS2_PLACEMENT_3D('',#7271,#5842,#5843);
#5164=AXIS2_PLACEMENT_3D('',#7272,#5844,#5845);
#5826=DIRECTION('axis',(0.,0.,1.));
#5827=DIRECTION('refdir',(1.,0.,0.));
#5828=DIRECTION('center_axis',(0.,0.,1.));
#5829=DIRECTION('ref_axis',(1.,0.,0.));
#5830=DIRECTION('center_axis',(0.,0.,-1.));
#5831=DIRECTION('ref_axis',(1.,0.,0.));
#5832=DIRECTION('',(0.,0.,-1.));
#5833=DIRECTION('center_axis',(0.,0.,-1.));
#5834=DIRECTION('ref_axis',(1.,0.,0.));
#5835=DIRECTION('center_axis',(0.,0.,1.));
#5836=DIRECTION('ref_axis',(1.,0.,0.));
#5837=DIRECTION('center_axis',(0.,0.,1.));
#5838=DIRECTION('ref_axis',(1.,0.,0.));
#5839=DIRECTION('',(0.,0.,-1.));
#5840=DIRECTION('center_axis',(0.,0.,1.));
#5841=DIRECTION('ref_axis',(1.,0.,0.));
#5842=DIRECTION('center_axis',(0.,0.,1.));
#5843=DIRECTION('ref_axis',(1.,0.,0.));
#5844=DIRECTION('center_axis',(0.,0.,1.));
#5845=DIRECTION('ref_axis',(1.,0.,0.));
#7258=CARTESIAN_POINT('',(0.,0.,0.));
#7259=CARTESIAN_POINT('Origin',(4.75,0.,3.2));
#7260=CARTESIAN_POINT('',(4.325,-5.20474889637625E-17,4.4));
#7261=CARTESIAN_POINT('Origin',(4.75,0.,4.4));
#7262=CARTESIAN_POINT('',(4.325,-5.20474889637625E-17,3.2));
#7263=CARTESIAN_POINT('',(4.325,-5.20474889637625E-17,3.2));
#7264=CARTESIAN_POINT('Origin',(4.75,0.,3.2));
#7265=CARTESIAN_POINT('Origin',(4.75,0.,3.2));
#7266=CARTESIAN_POINT('',(4.105,-7.89897185450042E-17,4.4));
#7267=CARTESIAN_POINT('Origin',(4.75,0.,4.4));
#7268=CARTESIAN_POINT('',(4.105,-7.89897185450042E-17,3.2));
#7269=CARTESIAN_POINT('',(4.105,-7.89897185450042E-17,3.2));
#7270=CARTESIAN_POINT('Origin',(4.75,0.,3.2));
#7271=CARTESIAN_POINT('Origin',(4.75,0.,4.4));
#7272=CARTESIAN_POINT('Origin',(4.75,0.,3.2));
#9083=UNCERTAINTY_MEASURE_WITH_UNIT(LENGTH_MEASURE(0.001),#9142,
'DISTANCE_ACCURACY_VALUE',
'Maximum model space distance between geometric entities at asserted c
onnectivities');
#9108=UNCERTAINTY_MEASURE_WITH_UNIT(LENGTH_MEASURE(0.001),#9142,
'DISTANCE_ACCURACY_VALUE',
'Maximum model space distance between geometric entities at asserted c
onnectivities');
#9116=(
GEOMETRIC_REPRESENTATION_CONTEXT(3)
GLOBAL_UNCERTAINTY_ASSIGNED_CONTEXT((#9083))
GLOBAL_UNIT_ASSIGNED_CONTEXT((#9142,#9144,#9145))
REPRESENTATION_CONTEXT('','3D')
);
#9141=(
GEOMETRIC_REPRESENTATION_CONTEXT(3)
GLOBAL_UNCERTAINTY_ASSIGNED_CONTEXT((#9108))
GLOBAL_UNIT_ASSIGNED_CONTEXT((#9142,#9144,#9145))
REPRESENTATION_CONTEXT('','3D')
);
#9142=(
LENGTH_UNIT()
NAMED_UNIT(*)
SI_UNIT(.CENTI.,.METRE.)
);
#9144=(
NAMED_UNIT(*)
PLANE_ANGLE_UNIT()
SI_UNIT($,.RADIAN.)
);
#9145=(
NAMED_UNIT(*)
SI_UNIT($,.STERADIAN.)
SOLID_ANGLE_UNIT()
);
#9153=SHAPE_DEFINITION_REPRESENTATION(#9185,#9281);
#9185=PRODUCT_DEFINITION_SHAPE('',$,#9314);
#9281=SHAPE_REPRESENTATION('',(#5156),#9116);
#9306=PRODUCT_DEFINITION_CONTEXT('part definition',#9404,'design');
#9314=PRODUCT_DEFINITION('Mounting bush (1)','Mounting bush (1)',#9346,#9306);
#9346=PRODUCT_DEFINITION_FORMATION('',$,#9413);
#9404=APPLICATION_CONTEXT(
'Core Data for Automotive Mechanical Design Process');
#9405=PRODUCT_CONTEXT('part definition',#9404,'mechanical');
#9413=PRODUCT('Mounting bush (1)','Mounting bush (1)','Mounting bush (1)',(#9405));
#9487=COLOUR_RGB('Sky Blue',0.24,0.69,0.87);
#9488=FILL_AREA_STYLE_COLOUR('',#9487);
#9489=FILL_AREA_STYLE('',(#9488));
#9490=SURFACE_STYLE_FILL_AREA(#9489);
#9491=SURFACE_SIDE_STYLE('',(#9490));
#9492=SURFACE_STYLE_USAGE(.BOTH.,#9491);
#9493=PRESENTATION_STYLE_ASSIGNMENT((#9492));
ENDSEC;
END-ISO-10303-21;
